ISO-10303-21;
HEADER;
/* Generated by software containing ST-Developer
 * from STEP Tools, Inc. (www.steptools.com) 
 */

FILE_DESCRIPTION(
/* description */ ('Compact handwheel screw vise'),
/* implementation_level */ '2;1');

FILE_NAME(
/* name */ 'M6x20 trimmed screw.step',
/* time_stamp */ '2026-10-29T16:08:22-07:00',
/* author */ (''),
/* organization */ (''),
/* preprocessor_version */ 'ST-DEVELOPER v20.2',
/* originating_system */ 'Autodesk Translation Framework v15.17.0.0',
/* authorisation */ '');

FILE_SCHEMA (('AUTOMOTIVE_DESIGN { 1 0 10303 214 3 1 1 }'));
ENDSEC;

DATA;
#10=MECHANICAL_DESIGN_GEOMETRIC_PRESENTATION_REPRESENTATION('',(#650),#25074);
#559=CONICAL_SURFACE('',#8561,0.475,0.785398163397449);
#560=CONICAL_SURFACE('',#8565,0.485,0.785398163397448);
#561=CONICAL_SURFACE('',#8569,0.31,0.463647609000806);
#580=ORIENTED_CLOSED_SHELL('',*,#8058,.F.);
#584=BREP_WITH_VOIDS('Body1',#8059,(#580));
#594=SHAPE_REPRESENTATION_RELATIONSHIP('SRR','None',#25202,#622);
#622=ADVANCED_BREP_SHAPE_REPRESENTATION('',(#584),#25049);
#650=STYLED_ITEM('',(#25446),#584);
#759=FACE_BOUND('',#1620,.T.);
#868=PLANE('',#8549);
#869=PLANE('',#8550);
#870=PLANE('',#8551);
#871=PLANE('',#8552);
#872=PLANE('',#8553);
#873=PLANE('',#8554);
#874=PLANE('',#8555);
#875=PLANE('',#8556);
#876=PLANE('',#8557);
#877=PLANE('',#8559);
#878=PLANE('',#8567);
#1089=FACE_OUTER_BOUND('',#1606,.T.);
#1090=FACE_OUTER_BOUND('',#1607,.T.);
#1091=FACE_OUTER_BOUND('',#1608,.T.);
#1092=FACE_OUTER_BOUND('',#1609,.T.);
#1093=FACE_OUTER_BOUND('',#1610,.T.);
#1094=FACE_OUTER_BOUND('',#1611,.T.);
#1095=FACE_OUTER_BOUND('',#1612,.T.);
#1096=FACE_OUTER_BOUND('',#1613,.T.);
#1097=FACE_OUTER_BOUND('',#1614,.T.);
#1098=FACE_OUTER_BOUND('',#1615,.T.);
#1099=FACE_OUTER_BOUND('',#1616,.T.);
#1100=FACE_OUTER_BOUND('',#1617,.T.);
#1101=FACE_OUTER_BOUND('',#1618,.T.);
#1102=FACE_OUTER_BOUND('',#1619,.T.);
#1103=FACE_OUTER_BOUND('',#1621,.T.);
#1104=FACE_OUTER_BOUND('',#1622,.T.);
#1606=EDGE_LOOP('',(#5471,#5472,#5473,#5474));
#1607=EDGE_LOOP('',(#5475,#5476,#5477,#5478));
#1608=EDGE_LOOP('',(#5479,#5480,#5481,#5482));
#1609=EDGE_LOOP('',(#5483,#5484,#5485,#5486));
#1610=EDGE_LOOP('',(#5487,#5488,#5489,#5490));
#1611=EDGE_LOOP('',(#5491,#5492,#5493,#5494));
#1612=EDGE_LOOP('',(#5495,#5496,#5497,#5498,#5499,#5500));
#1613=EDGE_LOOP('',(#5501,#5502,#5503,#5504,#5505,#5506));
#1614=EDGE_LOOP('',(#5507));
#1615=EDGE_LOOP('',(#5508));
#1616=EDGE_LOOP('',(#5509,#5510,#5511,#5512));
#1617=EDGE_LOOP('',(#5513,#5514,#5515,#5516));
#1618=EDGE_LOOP('',(#5517,#5518,#5519,#5520));
#1619=EDGE_LOOP('',(#5521));
#1620=EDGE_LOOP('',(#5522));
#1621=EDGE_LOOP('',(#5523,#5524,#5525,#5526));
#1622=EDGE_LOOP('',(#5527,#5528,#5529,#5530));
#2156=LINE('',#11667,#2664);
#2157=LINE('',#11669,#2665);
#2158=LINE('',#11671,#2666);
#2159=LINE('',#11672,#2667);
#2160=LINE('',#11675,#2668);
#2161=LINE('',#11677,#2669);
#2162=LINE('',#11678,#2670);
#2163=LINE('',#11681,#2671);
#2164=LINE('',#11683,#2672);
#2165=LINE('',#11684,#2673);
#2166=LINE('',#11687,#2674);
#2167=LINE('',#11689,#2675);
#2168=LINE('',#11690,#2676);
#2169=LINE('',#11693,#2677);
#2170=LINE('',#11695,#2678);
#2171=LINE('',#11696,#2679);
#2172=LINE('',#11698,#2680);
#2173=LINE('',#11699,#2681);
#2174=LINE('',#11711,#2682);
#2175=LINE('',#11715,#2683);
#2176=LINE('',#11719,#2684);
#2177=LINE('',#11726,#2685);
#2178=LINE('',#11728,#2686);
#2664=VECTOR('',#9596,1.);
#2665=VECTOR('',#9597,1.);
#2666=VECTOR('',#9598,1.);
#2667=VECTOR('',#9599,1.);
#2668=VECTOR('',#9602,1.);
#2669=VECTOR('',#9603,1.);
#2670=VECTOR('',#9604,1.);
#2671=VECTOR('',#9607,1.);
#2672=VECTOR('',#9608,1.);
#2673=VECTOR('',#9609,1.);
#2674=VECTOR('',#9612,1.);
#2675=VECTOR('',#9613,1.);
#2676=VECTOR('',#9614,1.);
#2677=VECTOR('',#9617,1.);
#2678=VECTOR('',#9618,1.);
#2679=VECTOR('',#9619,1.);
#2680=VECTOR('',#9622,1.);
#2681=VECTOR('',#9623,1.);
#2682=VECTOR('',#9640,0.475);
#2683=VECTOR('',#9645,0.5);
#2684=VECTOR('',#9650,0.485);
#2685=VECTOR('',#9659,0.31);
#2686=VECTOR('',#9662,0.3);
#3140=CIRCLE('',#8558,0.2942);
#3141=CIRCLE('',#8560,0.45);
#3142=CIRCLE('',#8562,0.5);
#3143=CIRCLE('',#8564,0.5);
#3144=CIRCLE('',#8566,0.47);
#3145=CIRCLE('',#8568,0.32);
#3146=CIRCLE('',#8570,0.2942);
#3437=VERTEX_POINT('',#11665);
#3438=VERTEX_POINT('',#11666);
#3439=VERTEX_POINT('',#11668);
#3440=VERTEX_POINT('',#11670);
#3441=VERTEX_POINT('',#11674);
#3442=VERTEX_POINT('',#11676);
#3443=VERTEX_POINT('',#11680);
#3444=VERTEX_POINT('',#11682);
#3445=VERTEX_POINT('',#11686);
#3446=VERTEX_POINT('',#11688);
#3447=VERTEX_POINT('',#11692);
#3448=VERTEX_POINT('',#11694);
#3449=VERTEX_POINT('',#11703);
#3450=VERTEX_POINT('',#11706);
#3451=VERTEX_POINT('',#11709);
#3452=VERTEX_POINT('',#11713);
#3453=VERTEX_POINT('',#11717);
#3454=VERTEX_POINT('',#11721);
#3455=VERTEX_POINT('',#11724);
#4222=EDGE_CURVE('',#3437,#3438,#2156,.T.);
#4223=EDGE_CURVE('',#3438,#3439,#2157,.T.);
#4224=EDGE_CURVE('',#3439,#3440,#2158,.T.);
#4225=EDGE_CURVE('',#3437,#3440,#2159,.T.);
#4226=EDGE_CURVE('',#3438,#3441,#2160,.T.);
#4227=EDGE_CURVE('',#3441,#3442,#2161,.T.);
#4228=EDGE_CURVE('',#3442,#3439,#2162,.T.);
#4229=EDGE_CURVE('',#3441,#3443,#2163,.T.);
#4230=EDGE_CURVE('',#3443,#3444,#2164,.T.);
#4231=EDGE_CURVE('',#3444,#3442,#2165,.T.);
#4232=EDGE_CURVE('',#3443,#3445,#2166,.T.);
#4233=EDGE_CURVE('',#3445,#3446,#2167,.T.);
#4234=EDGE_CURVE('',#3446,#3444,#2168,.T.);
#4235=EDGE_CURVE('',#3445,#3447,#2169,.T.);
#4236=EDGE_CURVE('',#3447,#3448,#2170,.T.);
#4237=EDGE_CURVE('',#3448,#3446,#2171,.T.);
#4238=EDGE_CURVE('',#3447,#3437,#2172,.T.);
#4239=EDGE_CURVE('',#3440,#3448,#2173,.T.);
#4240=EDGE_CURVE('',#3449,#3449,#3140,.T.);
#4241=EDGE_CURVE('',#3450,#3450,#3141,.T.);
#4242=EDGE_CURVE('',#3451,#3451,#3142,.T.);
#4243=EDGE_CURVE('',#3451,#3450,#2174,.T.);
#4244=EDGE_CURVE('',#3452,#3452,#3143,.T.);
#4245=EDGE_CURVE('',#3452,#3451,#2175,.T.);
#4246=EDGE_CURVE('',#3453,#3453,#3144,.T.);
#4247=EDGE_CURVE('',#3453,#3452,#2176,.T.);
#4248=EDGE_CURVE('',#3454,#3454,#3145,.T.);
#4249=EDGE_CURVE('',#3455,#3455,#3146,.F.);
#4250=EDGE_CURVE('',#3455,#3454,#2177,.T.);
#4251=EDGE_CURVE('',#3449,#3455,#2178,.T.);
#5471=ORIENTED_EDGE('',*,*,#4222,.T.);
#5472=ORIENTED_EDGE('',*,*,#4223,.T.);
#5473=ORIENTED_EDGE('',*,*,#4224,.T.);
#5474=ORIENTED_EDGE('',*,*,#4225,.F.);
#5475=ORIENTED_EDGE('',*,*,#4226,.T.);
#5476=ORIENTED_EDGE('',*,*,#4227,.T.);
#5477=ORIENTED_EDGE('',*,*,#4228,.T.);
#5478=ORIENTED_EDGE('',*,*,#4223,.F.);
#5479=ORIENTED_EDGE('',*,*,#4229,.T.);
#5480=ORIENTED_EDGE('',*,*,#4230,.T.);
#5481=ORIENTED_EDGE('',*,*,#4231,.T.);
#5482=ORIENTED_EDGE('',*,*,#4227,.F.);
#5483=ORIENTED_EDGE('',*,*,#4232,.T.);
#5484=ORIENTED_EDGE('',*,*,#4233,.T.);
#5485=ORIENTED_EDGE('',*,*,#4234,.T.);
#5486=ORIENTED_EDGE('',*,*,#4230,.F.);
#5487=ORIENTED_EDGE('',*,*,#4235,.T.);
#5488=ORIENTED_EDGE('',*,*,#4236,.T.);
#5489=ORIENTED_EDGE('',*,*,#4237,.T.);
#5490=ORIENTED_EDGE('',*,*,#4233,.F.);
#5491=ORIENTED_EDGE('',*,*,#4238,.T.);
#5492=ORIENTED_EDGE('',*,*,#4225,.T.);
#5493=ORIENTED_EDGE('',*,*,#4239,.T.);
#5494=ORIENTED_EDGE('',*,*,#4236,.F.);
#5495=ORIENTED_EDGE('',*,*,#4238,.F.);
#5496=ORIENTED_EDGE('',*,*,#4235,.F.);
#5497=ORIENTED_EDGE('',*,*,#4232,.F.);
#5498=ORIENTED_EDGE('',*,*,#4229,.F.);
#5499=ORIENTED_EDGE('',*,*,#4226,.F.);
#5500=ORIENTED_EDGE('',*,*,#4222,.F.);
#5501=ORIENTED_EDGE('',*,*,#4239,.F.);
#5502=ORIENTED_EDGE('',*,*,#4224,.F.);
#5503=ORIENTED_EDGE('',*,*,#4228,.F.);
#5504=ORIENTED_EDGE('',*,*,#4231,.F.);
#5505=ORIENTED_EDGE('',*,*,#4234,.F.);
#5506=ORIENTED_EDGE('',*,*,#4237,.F.);
#5507=ORIENTED_EDGE('',*,*,#4240,.F.);
#5508=ORIENTED_EDGE('',*,*,#4241,.F.);
#5509=ORIENTED_EDGE('',*,*,#4242,.F.);
#5510=ORIENTED_EDGE('',*,*,#4243,.T.);
#5511=ORIENTED_EDGE('',*,*,#4241,.T.);
#5512=ORIENTED_EDGE('',*,*,#4243,.F.);
#5513=ORIENTED_EDGE('',*,*,#4244,.F.);
#5514=ORIENTED_EDGE('',*,*,#4245,.T.);
#5515=ORIENTED_EDGE('',*,*,#4242,.T.);
#5516=ORIENTED_EDGE('',*,*,#4245,.F.);
#5517=ORIENTED_EDGE('',*,*,#4246,.F.);
#5518=ORIENTED_EDGE('',*,*,#4247,.T.);
#5519=ORIENTED_EDGE('',*,*,#4244,.T.);
#5520=ORIENTED_EDGE('',*,*,#4247,.F.);
#5521=ORIENTED_EDGE('',*,*,#4246,.T.);
#5522=ORIENTED_EDGE('',*,*,#4248,.F.);
#5523=ORIENTED_EDGE('',*,*,#4249,.F.);
#5524=ORIENTED_EDGE('',*,*,#4250,.T.);
#5525=ORIENTED_EDGE('',*,*,#4248,.T.);
#5526=ORIENTED_EDGE('',*,*,#4250,.F.);
#5527=ORIENTED_EDGE('',*,*,#4240,.T.);
#5528=ORIENTED_EDGE('',*,*,#4251,.T.);
#5529=ORIENTED_EDGE('',*,*,#4249,.T.);
#5530=ORIENTED_EDGE('',*,*,#4251,.F.);
#7376=CYLINDRICAL_SURFACE('',#8563,0.5);
#7377=CYLINDRICAL_SURFACE('',#8571,0.2942);
#7659=ADVANCED_FACE('',(#1089),#868,.F.);
#7660=ADVANCED_FACE('',(#1090),#869,.F.);
#7661=ADVANCED_FACE('',(#1091),#870,.F.);
#7662=ADVANCED_FACE('',(#1092),#871,.F.);
#7663=ADVANCED_FACE('',(#1093),#872,.F.);
#7664=ADVANCED_FACE('',(#1094),#873,.F.);
#7665=ADVANCED_FACE('',(#1095),#874,.F.);
#7666=ADVANCED_FACE('',(#1096),#875,.F.);
#7667=ADVANCED_FACE('',(#1097),#876,.F.);
#7668=ADVANCED_FACE('',(#1098),#877,.T.);
#7669=ADVANCED_FACE('',(#1099),#559,.T.);
#7670=ADVANCED_FACE('',(#1100),#7376,.T.);
#7671=ADVANCED_FACE('',(#1101),#560,.T.);
#7672=ADVANCED_FACE('',(#1102,#759),#878,.T.);
#7673=ADVANCED_FACE('',(#1103),#561,.T.);
#7674=ADVANCED_FACE('',(#1104),#7377,.T.);
#8058=CLOSED_SHELL('',(#7659,#7660,#7661,#7662,#7663,#7664,#7665,#7666));
#8059=CLOSED_SHELL('',(#7667,#7668,#7669,#7670,#7671,#7672,#7673,#7674));
#8548=AXIS2_PLACEMENT_3D('',#11663,#9592,#9593);
#8549=AXIS2_PLACEMENT_3D('',#11664,#9594,#9595);
#8550=AXIS2_PLACEMENT_3D('',#11673,#9600,#9601);
#8551=AXIS2_PLACEMENT_3D('',#11679,#9605,#9606);
#8552=AXIS2_PLACEMENT_3D('',#11685,#9610,#9611);
#8553=AXIS2_PLACEMENT_3D('',#11691,#9615,#9616);
#8554=AXIS2_PLACEMENT_3D('',#11697,#9620,#9621);
#8555=AXIS2_PLACEMENT_3D('',#11700,#9624,#9625);
#8556=AXIS2_PLACEMENT_3D('',#11701,#9626,#9627);
#8557=AXIS2_PLACEMENT_3D('',#11702,#9628,#9629);
#8558=AXIS2_PLACEMENT_3D('',#11704,#9630,#9631);
#8559=AXIS2_PLACEMENT_3D('',#11705,#9632,#9633);
#8560=AXIS2_PLACEMENT_3D('',#11707,#9634,#9635);
#8561=AXIS2_PLACEMENT_3D('',#11708,#9636,#9637);
#8562=AXIS2_PLACEMENT_3D('',#11710,#9638,#9639);
#8563=AXIS2_PLACEMENT_3D('',#11712,#9641,#9642);
#8564=AXIS2_PLACEMENT_3D('',#11714,#9643,#9644);
#8565=AXIS2_PLACEMENT_3D('',#11716,#9646,#9647);
#8566=AXIS2_PLACEMENT_3D('',#11718,#9648,#9649);
#8567=AXIS2_PLACEMENT_3D('',#11720,#9651,#9652);
#8568=AXIS2_PLACEMENT_3D('',#11722,#9653,#9654);
#8569=AXIS2_PLACEMENT_3D('',#11723,#9655,#9656);
#8570=AXIS2_PLACEMENT_3D('',#11725,#9657,#9658);
#8571=AXIS2_PLACEMENT_3D('',#11727,#9660,#9661);
#9592=DIRECTION('axis',(0.,0.,1.));
#9593=DIRECTION('refdir',(1.,0.,0.));
#9594=DIRECTION('center_axis',(0.866025403784439,0.,-0.5));
#9595=DIRECTION('ref_axis',(0.5,0.,0.866025403784439));
#9596=DIRECTION('',(-0.5,0.,-0.866025403784439));
#9597=DIRECTION('',(0.,-1.,0.));
#9598=DIRECTION('',(0.5,0.,0.866025403784439));
#9599=DIRECTION('',(0.,-1.,0.));
#9600=DIRECTION('center_axis',(1.92296268638356E-16,0.,-1.));
#9601=DIRECTION('ref_axis',(1.,0.,1.92296268638356E-16));
#9602=DIRECTION('',(-1.,0.,-1.92296268638356E-16));
#9603=DIRECTION('',(0.,-1.,0.));
#9604=DIRECTION('',(1.,0.,1.92296268638356E-16));
#9605=DIRECTION('center_axis',(-0.866025403784439,0.,-0.5));
#9606=DIRECTION('ref_axis',(0.5,0.,-0.866025403784439));
#9607=DIRECTION('',(-0.5,0.,0.866025403784438));
#9608=DIRECTION('',(0.,-1.,0.));
#9609=DIRECTION('',(0.5,0.,-0.866025403784438));
#9610=DIRECTION('center_axis',(-0.866025403784439,0.,0.5));
#9611=DIRECTION('ref_axis',(-0.5,0.,-0.866025403784439));
#9612=DIRECTION('',(0.5,0.,0.866025403784439));
#9613=DIRECTION('',(0.,-1.,0.));
#9614=DIRECTION('',(-0.5,0.,-0.866025403784439));
#9615=DIRECTION('center_axis',(-1.92296268638356E-16,0.,1.));
#9616=DIRECTION('ref_axis',(-1.,0.,-1.92296268638356E-16));
#9617=DIRECTION('',(1.,0.,1.92296268638356E-16));
#9618=DIRECTION('',(0.,-1.,0.));
#9619=DIRECTION('',(-1.,0.,-1.92296268638356E-16));
#9620=DIRECTION('center_axis',(0.866025403784439,0.,0.5));
#9621=DIRECTION('ref_axis',(-0.5,0.,0.866025403784439));
#9622=DIRECTION('',(0.5,0.,-0.866025403784439));
#9623=DIRECTION('',(-0.5,0.,0.866025403784439));
#9624=DIRECTION('center_axis',(0.,1.,0.));
#9625=DIRECTION('ref_axis',(1.,0.,0.));
#9626=DIRECTION('center_axis',(0.,-1.,0.));
#9627=DIRECTION('ref_axis',(0.,0.,-1.));
#9628=DIRECTION('center_axis',(0.,1.,0.));
#9629=DIRECTION('ref_axis',(1.,0.,0.));
#9630=DIRECTION('center_axis',(0.,1.,0.));
#9631=DIRECTION('ref_axis',(1.,0.,0.));
#9632=DIRECTION('center_axis',(0.,1.,0.));
#9633=DIRECTION('ref_axis',(0.,0.,1.));
#9634=DIRECTION('center_axis',(0.,-1.,0.));
#9635=DIRECTION('ref_axis',(1.,0.,0.));
#9636=DIRECTION('center_axis',(0.,-1.,0.));
#9637=DIRECTION('ref_axis',(1.,0.,0.));
#9638=DIRECTION('center_axis',(0.,-1.,0.));
#9639=DIRECTION('ref_axis',(1.,0.,0.));
#9640=DIRECTION('',(0.707106781186548,0.707106781186547,8.65956056235494E-17));
#9641=DIRECTION('center_axis',(0.,-1.,0.));
#9642=DIRECTION('ref_axis',(1.,0.,0.));
#9643=DIRECTION('center_axis',(0.,-1.,0.));
#9644=DIRECTION('ref_axis',(1.,0.,0.));
#9645=DIRECTION('',(0.,1.,0.));
#9646=DIRECTION('center_axis',(0.,1.,0.));
#9647=DIRECTION('ref_axis',(1.,0.,0.));
#9648=DIRECTION('center_axis',(0.,-1.,0.));
#9649=DIRECTION('ref_axis',(1.,0.,0.));
#9650=DIRECTION('',(-0.707106781186547,0.707106781186548,-8.65956056235493E-17));
#9651=DIRECTION('center_axis',(0.,-1.,0.));
#9652=DIRECTION('ref_axis',(0.,0.,-1.));
#9653=DIRECTION('center_axis',(0.,-1.,0.));
#9654=DIRECTION('ref_axis',(1.,0.,0.));
#9655=DIRECTION('center_axis',(0.,1.,0.));
#9656=DIRECTION('ref_axis',(1.,0.,0.));
#9657=DIRECTION('center_axis',(0.,1.,0.));
#9658=DIRECTION('ref_axis',(1.,0.,0.));
#9659=DIRECTION('',(-0.447213595499958,0.894427190999916,-5.47678698264203E-17));
#9660=DIRECTION('center_axis',(0.,-1.,0.));
#9661=DIRECTION('ref_axis',(1.,0.,0.));
#9662=DIRECTION('',(0.,1.,0.));
#11663=CARTESIAN_POINT('',(0.,0.,0.));
#11664=CARTESIAN_POINT('Origin',(0.144337567297406,-0.6,-0.25));
#11665=CARTESIAN_POINT('',(0.288675134594813,-0.6,0.));
#11666=CARTESIAN_POINT('',(0.144337567297406,-0.6,-0.25));
#11667=CARTESIAN_POINT('',(0.288675134594813,-0.6,0.));
#11668=CARTESIAN_POINT('',(0.144337567297406,-0.96,-0.25));
#11669=CARTESIAN_POINT('',(0.144337567297406,-0.6,-0.25));
#11670=CARTESIAN_POINT('',(0.288675134594813,-0.96,0.));
#11671=CARTESIAN_POINT('',(0.288675134594813,-0.96,0.));
#11672=CARTESIAN_POINT('',(0.288675134594813,-0.6,0.));
#11673=CARTESIAN_POINT('Origin',(-0.144337567297406,-0.6,-0.25));
#11674=CARTESIAN_POINT('',(-0.144337567297406,-0.6,-0.25));
#11675=CARTESIAN_POINT('',(0.144337567297406,-0.6,-0.25));
#11676=CARTESIAN_POINT('',(-0.144337567297406,-0.96,-0.25));
#11677=CARTESIAN_POINT('',(-0.144337567297406,-0.6,-0.25));
#11678=CARTESIAN_POINT('',(0.144337567297406,-0.96,-0.25));
#11679=CARTESIAN_POINT('Origin',(-0.288675134594813,-0.6,-8.32667268468867E-17));
#11680=CARTESIAN_POINT('',(-0.288675134594813,-0.6,-3.53525079574969E-17));
#11681=CARTESIAN_POINT('',(-0.144337567297406,-0.6,-0.25));
#11682=CARTESIAN_POINT('',(-0.288675134594813,-0.96,-5.55111512312578E-17));
#11683=CARTESIAN_POINT('',(-0.288675134594813,-0.6,-3.53525079574969E-17));
#11684=CARTESIAN_POINT('',(-0.144337567297406,-0.96,-0.25));
#11685=CARTESIAN_POINT('Origin',(-0.144337567297407,-0.6,0.25));
#11686=CARTESIAN_POINT('',(-0.144337567297407,-0.6,0.25));
#11687=CARTESIAN_POINT('',(-0.288675134594813,-0.6,-3.53525079574969E-17));
#11688=CARTESIAN_POINT('',(-0.144337567297407,-0.96,0.25));
#11689=CARTESIAN_POINT('',(-0.144337567297407,-0.6,0.25));
#11690=CARTESIAN_POINT('',(-0.288675134594813,-0.96,-3.53525079574969E-17));
#11691=CARTESIAN_POINT('Origin',(0.144337567297406,-0.6,0.25));
#11692=CARTESIAN_POINT('',(0.144337567297406,-0.6,0.25));
#11693=CARTESIAN_POINT('',(-0.144337567297407,-0.6,0.25));
#11694=CARTESIAN_POINT('',(0.144337567297406,-0.96,0.25));
#11695=CARTESIAN_POINT('',(0.144337567297406,-0.6,0.25));
#11696=CARTESIAN_POINT('',(-0.144337567297407,-0.96,0.25));
#11697=CARTESIAN_POINT('Origin',(0.288675134594813,-0.6,0.));
#11698=CARTESIAN_POINT('',(0.144337567297406,-0.6,0.25));
#11699=CARTESIAN_POINT('',(0.144337567297406,-0.96,0.25));
#11700=CARTESIAN_POINT('Origin',(0.,-0.6,0.));
#11701=CARTESIAN_POINT('Origin',(0.,-0.96,0.));
#11702=CARTESIAN_POINT('Origin',(0.,-2.,0.));
#11703=CARTESIAN_POINT('',(-0.2942,-2.,3.60291088309151E-17));
#11704=CARTESIAN_POINT('Origin',(0.,-2.,0.));
#11705=CARTESIAN_POINT('Origin',(0.45,0.6,0.));
#11706=CARTESIAN_POINT('',(-0.45,0.6,-5.51091059616309E-17));
#11707=CARTESIAN_POINT('Origin',(0.,0.6,0.));
#11708=CARTESIAN_POINT('Origin',(0.,0.575,0.));
#11709=CARTESIAN_POINT('',(-0.5,0.55,-6.12323399573677E-17));
#11710=CARTESIAN_POINT('Origin',(0.,0.55,0.));
#11711=CARTESIAN_POINT('',(-0.475,0.575,-5.81707229594993E-17));
#11712=CARTESIAN_POINT('Origin',(0.,0.29,0.));
#11713=CARTESIAN_POINT('',(-0.5,0.0299999999999998,-6.12323399573677E-17));
#11714=CARTESIAN_POINT('Origin',(0.,0.0299999999999998,0.));
#11715=CARTESIAN_POINT('',(-0.5,0.29,-6.12323399573677E-17));
#11716=CARTESIAN_POINT('Origin',(0.,0.0150000000000001,0.));
#11717=CARTESIAN_POINT('',(-0.47,7.11236625150491E-17,-5.75583995599256E-17));
#11718=CARTESIAN_POINT('Origin',(0.,0.,0.));
#11719=CARTESIAN_POINT('',(-0.485,0.0150000000000001,-5.93953697586466E-17));
#11720=CARTESIAN_POINT('Origin',(0.32,0.,0.));
#11721=CARTESIAN_POINT('',(-0.32,-6.93889390390723E-18,-3.91886975727153E-17));
#11722=CARTESIAN_POINT('Origin',(0.,0.,0.));
#11723=CARTESIAN_POINT('Origin',(0.,-0.02,0.));
#11724=CARTESIAN_POINT('',(-0.2942,-0.0515999999999999,3.60291088309151E-17));
#11725=CARTESIAN_POINT('Origin',(0.,-0.0515999999999999,0.));
#11726=CARTESIAN_POINT('',(-0.31,-0.02,-3.7964050773568E-17));
#11727=CARTESIAN_POINT('Origin',(0.,-1.24,0.));
#11728=CARTESIAN_POINT('',(-0.2942,-1.24,-3.60291088309151E-17));
#25015=UNCERTAINTY_MEASURE_WITH_UNIT(LENGTH_MEASURE(0.001),#25075,
'DISTANCE_ACCURACY_VALUE',
'Maximum model space distance between geometric entities at asserted c
onnectivities');
#25040=UNCERTAINTY_MEASURE_WITH_UNIT(LENGTH_MEASURE(0.001),#25075,
'DISTANCE_ACCURACY_VALUE',
'Maximum model space distance between geometric entities at asserted c
onnectivities');
#25049=(
GEOMETRIC_REPRESENTATION_CONTEXT(3)
GLOBAL_UNCERTAINTY_ASSIGNED_CONTEXT((#25015))
GLOBAL_UNIT_ASSIGNED_CONTEXT((#25075,#25077,#25078))
REPRESENTATION_CONTEXT('','3D')
);
#25074=(
GEOMETRIC_REPRESENTATION_CONTEXT(3)
GLOBAL_UNCERTAINTY_ASSIGNED_CONTEXT((#25040))
GLOBAL_UNIT_ASSIGNED_CONTEXT((#25075,#25077,#25078))
REPRESENTATION_CONTEXT('','3D')
);
#25075=(
LENGTH_UNIT()
NAMED_UNIT(*)
SI_UNIT(.CENTI.,.METRE.)
);
#25077=(
NAMED_UNIT(*)
PLANE_ANGLE_UNIT()
SI_UNIT($,.RADIAN.)
);
#25078=(
NAMED_UNIT(*)
SI_UNIT($,.STERADIAN.)
SOLID_ANGLE_UNIT()
);
#25087=SHAPE_DEFINITION_REPRESENTATION(#25120,#25202);
#25120=PRODUCT_DEFINITION_SHAPE('',$,#25236);
#25202=SHAPE_REPRESENTATION('',(#8548),#25049);
#25227=PRODUCT_DEFINITION_CONTEXT('part definition',#25328,'design');
#25236=PRODUCT_DEFINITION('M6x20 trimmed screw','M6x20 trimmed screw',#25269,
#25227);
#25269=PRODUCT_DEFINITION_FORMATION('',$,#25338);
#25328=APPLICATION_CONTEXT(
'Core Data for Automotive Mechanical Design Process');
#25329=PRODUCT_CONTEXT('part definition',#25328,'mechanical');
#25338=PRODUCT('M6x20 trimmed screw','M6x20 trimmed screw',
'M6x20 trimmed screw',(#25329));
#25440=COLOUR_RGB('Black',0.12,0.14,0.17);
#25441=FILL_AREA_STYLE_COLOUR('',#25440);
#25442=FILL_AREA_STYLE('',(#25441));
#25443=SURFACE_STYLE_FILL_AREA(#25442);
#25444=SURFACE_SIDE_STYLE('',(#25443));
#25445=SURFACE_STYLE_USAGE(.BOTH.,#25444);
#25446=PRESENTATION_STYLE_ASSIGNMENT((#25445));
ENDSEC;
END-ISO-10303-21;
